ISO-10303-21;
HEADER;
/* Generated by software containing ST-Developer
 * from STEP Tools, Inc. (www.steptools.com) 
 */

FILE_DESCRIPTION(
/* description */ ('', 'CAx-IF Rec.Pracs.---Representation and Presentation of Product Manufa
cturing Information (PMI)---4.0---2014-10-13'),
/* implementation_level */ '2;1');

FILE_NAME(
/* name */ 'Extended Housing Socket Screw.step',
/* time_stamp */ '2026-10-28T23:00:48+01:00',
/* author */ (''),
/* organization */ (''),
/* preprocessor_version */ 'ST-DEVELOPER v20.2',
/* originating_system */ 'Autodesk Translation Framework v15.17.0.0',
/* authorisation */ '');

FILE_SCHEMA (('AP242_MANAGED_MODEL_BASED_3D_ENGINEERING_MIM_LF { 1 0 10303 442 2 1 4 }'));
ENDSEC;

DATA;
#10=MECHANICAL_DESIGN_GEOMETRIC_PRESENTATION_REPRESENTATION('',(#965),#61811);
#490=(
BOUNDED_CURVE()
B_SPLINE_CURVE(2,(#51187,#51188,#51189),.UNSPECIFIED.,.F.,.F.)
B_SPLINE_CURVE_WITH_KNOTS((3,3),(0.,0.467374455231167),.UNSPECIFIED.)
CURVE()
GEOMETRIC_REPRESENTATION_ITEM()
RATIONAL_B_SPLINE_CURVE((1.,1.15470053837925,1.))
REPRESENTATION_ITEM('')
);
#491=(
BOUNDED_CURVE()
B_SPLINE_CURVE(2,(#51194,#51195,#51196),.UNSPECIFIED.,.F.,.F.)
B_SPLINE_CURVE_WITH_KNOTS((3,3),(0.,0.467374455231167),.UNSPECIFIED.)
CURVE()
GEOMETRIC_REPRESENTATION_ITEM()
RATIONAL_B_SPLINE_CURVE((1.,1.15470053837925,1.))
REPRESENTATION_ITEM('')
);
#492=(
BOUNDED_CURVE()
B_SPLINE_CURVE(2,(#51200,#51201,#51202),.UNSPECIFIED.,.F.,.F.)
B_SPLINE_CURVE_WITH_KNOTS((3,3),(0.,0.467374455231166),.UNSPECIFIED.)
CURVE()
GEOMETRIC_REPRESENTATION_ITEM()
RATIONAL_B_SPLINE_CURVE((1.,1.15470053837925,1.))
REPRESENTATION_ITEM('')
);
#493=(
BOUNDED_CURVE()
B_SPLINE_CURVE(2,(#51206,#51207,#51208),.UNSPECIFIED.,.F.,.F.)
B_SPLINE_CURVE_WITH_KNOTS((3,3),(0.,0.467374455231167),.UNSPECIFIED.)
CURVE()
GEOMETRIC_REPRESENTATION_ITEM()
RATIONAL_B_SPLINE_CURVE((1.,1.15470053837926,1.))
REPRESENTATION_ITEM('')
);
#494=(
BOUNDED_CURVE()
B_SPLINE_CURVE(2,(#51212,#51213,#51214),.UNSPECIFIED.,.F.,.F.)
B_SPLINE_CURVE_WITH_KNOTS((3,3),(0.,0.233687227615584),.UNSPECIFIED.)
CURVE()
GEOMETRIC_REPRESENTATION_ITEM()
RATIONAL_B_SPLINE_CURVE((1.,1.07735026918963,1.07735026918963))
REPRESENTATION_ITEM('')
);
#495=(
BOUNDED_CURVE()
B_SPLINE_CURVE(2,(#51217,#51218,#51219),.UNSPECIFIED.,.F.,.F.)
B_SPLINE_CURVE_WITH_KNOTS((3,3),(0.233687227615584,0.467374455231167),
 .UNSPECIFIED.)
CURVE()
GEOMETRIC_REPRESENTATION_ITEM()
RATIONAL_B_SPLINE_CURVE((1.07735026918963,1.07735026918962,1.))
REPRESENTATION_ITEM('')
);
#496=(
BOUNDED_CURVE()
B_SPLINE_CURVE(2,(#51221,#51222,#51223),.UNSPECIFIED.,.F.,.F.)
B_SPLINE_CURVE_WITH_KNOTS((3,3),(0.,0.467374455231167),.UNSPECIFIED.)
CURVE()
GEOMETRIC_REPRESENTATION_ITEM()
RATIONAL_B_SPLINE_CURVE((1.,1.15470053837925,1.))
REPRESENTATION_ITEM('')
);
#569=CONICAL_SURFACE('',#34459,4.5399125,0.785398163397448);
#570=CONICAL_SURFACE('',#34475,2.3094010767585,1.0471975511966);
#892=TOROIDAL_SURFACE('',#34449,5.1,0.1);
#893=TOROIDAL_SURFACE('',#34462,7.,1.);
#915=SHAPE_REPRESENTATION_RELATIONSHIP('SRR','None',#61973,#940);
#940=ADVANCED_BREP_SHAPE_REPRESENTATION('',(#1004),#61786);
#965=STYLED_ITEM('',(#62163),#1004);
#1004=MANIFOLD_SOLID_BREP('Body1',#33795);
#1097=CYLINDRICAL_SURFACE('',#34454,5.);
#1098=CYLINDRICAL_SURFACE('',#34468,8.);
#1901=FACE_BOUND('',#6306,.T.);
#1902=FACE_BOUND('',#6311,.T.);
#2409=CIRCLE('',#34450,5.);
#2410=CIRCLE('',#34451,5.);
#2411=CIRCLE('',#34452,0.1);
#2412=CIRCLE('',#34453,5.1);
#2413=CIRCLE('',#34455,5.);
#2414=CIRCLE('',#34456,5.);
#2415=CIRCLE('',#34458,8.);
#2416=CIRCLE('',#34460,4.079825);
#2417=CIRCLE('',#34463,8.);
#2418=CIRCLE('',#34464,8.);
#2419=CIRCLE('',#34465,1.);
#2420=CIRCLE('',#34466,7.);
#4402=FACE_OUTER_BOUND('',#6303,.T.);
#4403=FACE_OUTER_BOUND('',#6304,.T.);
#4404=FACE_OUTER_BOUND('',#6305,.T.);
#4405=FACE_OUTER_BOUND('',#6307,.T.);
#4406=FACE_OUTER_BOUND('',#6308,.T.);
#4407=FACE_OUTER_BOUND('',#6309,.T.);
#4408=FACE_OUTER_BOUND('',#6310,.T.);
#4409=FACE_OUTER_BOUND('',#6312,.T.);
#4410=FACE_OUTER_BOUND('',#6313,.T.);
#4411=FACE_OUTER_BOUND('',#6314,.T.);
#4412=FACE_OUTER_BOUND('',#6315,.T.);
#4413=FACE_OUTER_BOUND('',#6316,.T.);
#4414=FACE_OUTER_BOUND('',#6317,.T.);
#4415=FACE_OUTER_BOUND('',#6318,.T.);
#4416=FACE_OUTER_BOUND('',#6319,.T.);
#6303=EDGE_LOOP('',(#22228,#22229,#22230,#22231,#22232));
#6304=EDGE_LOOP('',(#22233,#22234,#22235,#22236,#22237,#22238));
#6305=EDGE_LOOP('',(#22239));
#6306=EDGE_LOOP('',(#22240));
#6307=EDGE_LOOP('',(#22241,#22242,#22243,#22244,#22245));
#6308=EDGE_LOOP('',(#22246));
#6309=EDGE_LOOP('',(#22247,#22248,#22249,#22250,#22251));
#6310=EDGE_LOOP('',(#22252));
#6311=EDGE_LOOP('',(#22253,#22254,#22255,#22256,#22257,#22258));
#6312=EDGE_LOOP('',(#22259,#22260,#22261,#22262,#22263));
#6313=EDGE_LOOP('',(#22264,#22265,#22266,#22267));
#6314=EDGE_LOOP('',(#22268,#22269,#22270,#22271));
#6315=EDGE_LOOP('',(#22272,#22273,#22274,#22275));
#6316=EDGE_LOOP('',(#22276,#22277,#22278,#22279));
#6317=EDGE_LOOP('',(#22280,#22281,#22282,#22283,#22284));
#6318=EDGE_LOOP('',(#22285,#22286,#22287,#22288));
#6319=EDGE_LOOP('',(#22289,#22290,#22291,#22292,#22293,#22294,#22295,#22296,
#22297));
#8509=LINE('',#51152,#11056);
#8510=LINE('',#51158,#11057);
#8511=LINE('',#51172,#11058);
#8512=LINE('',#51174,#11059);
#8513=LINE('',#51176,#11060);
#8514=LINE('',#51178,#11061);
#8515=LINE('',#51180,#11062);
#8516=LINE('',#51181,#11063);
#8517=LINE('',#51183,#11064);
#8518=LINE('',#51190,#11065);
#8519=LINE('',#51191,#11066);
#8520=LINE('',#51197,#11067);
#8521=LINE('',#51203,#11068);
#8522=LINE('',#51209,#11069);
#8523=LINE('',#51216,#11070);
#8524=LINE('',#51226,#11071);
#11056=VECTOR('',#39019,5.);
#11057=VECTOR('',#39026,4.5399125);
#11058=VECTOR('',#39043,10.);
#11059=VECTOR('',#39044,10.);
#11060=VECTOR('',#39045,10.);
#11061=VECTOR('',#39046,10.);
#11062=VECTOR('',#39047,10.);
#11063=VECTOR('',#39048,10.);
#11064=VECTOR('',#39051,8.);
#11065=VECTOR('',#39054,10.);
#11066=VECTOR('',#39055,10.);
#11067=VECTOR('',#39058,10.);
#11068=VECTOR('',#39061,10.);
#11069=VECTOR('',#39064,10.);
#11070=VECTOR('',#39067,10.);
#11071=VECTOR('',#39072,2.3094010767585);
#13674=VERTEX_POINT('',#51140);
#13675=VERTEX_POINT('',#51141);
#13676=VERTEX_POINT('',#51144);
#13677=VERTEX_POINT('',#51148);
#13678=VERTEX_POINT('',#51149);
#13679=VERTEX_POINT('',#51154);
#13680=VERTEX_POINT('',#51157);
#13681=VERTEX_POINT('',#51162);
#13682=VERTEX_POINT('',#51163);
#13683=VERTEX_POINT('',#51166);
#13684=VERTEX_POINT('',#51170);
#13685=VERTEX_POINT('',#51171);
#13686=VERTEX_POINT('',#51173);
#13687=VERTEX_POINT('',#51175);
#13688=VERTEX_POINT('',#51177);
#13689=VERTEX_POINT('',#51179);
#13690=VERTEX_POINT('',#51185);
#13691=VERTEX_POINT('',#51186);
#13692=VERTEX_POINT('',#51193);
#13693=VERTEX_POINT('',#51199);
#13694=VERTEX_POINT('',#51205);
#13695=VERTEX_POINT('',#51211);
#13696=VERTEX_POINT('',#51215);
#13697=VERTEX_POINT('',#51225);
#17016=EDGE_CURVE('',#13674,#13675,#2409,.T.);
#17017=EDGE_CURVE('',#13675,#13674,#2410,.T.);
#17018=EDGE_CURVE('',#13674,#13676,#2411,.T.);
#17019=EDGE_CURVE('',#13676,#13676,#2412,.T.);
#17020=EDGE_CURVE('',#13677,#13678,#2413,.T.);
#17021=EDGE_CURVE('',#13678,#13677,#2414,.T.);
#17022=EDGE_CURVE('',#13678,#13675,#8509,.T.);
#17023=EDGE_CURVE('',#13679,#13679,#2415,.T.);
#17024=EDGE_CURVE('',#13677,#13680,#8510,.T.);
#17025=EDGE_CURVE('',#13680,#13680,#2416,.T.);
#17026=EDGE_CURVE('',#13681,#13682,#2417,.T.);
#17027=EDGE_CURVE('',#13682,#13681,#2418,.T.);
#17028=EDGE_CURVE('',#13681,#13683,#2419,.T.);
#17029=EDGE_CURVE('',#13683,#13683,#2420,.T.);
#17030=EDGE_CURVE('',#13684,#13685,#8511,.T.);
#17031=EDGE_CURVE('',#13685,#13686,#8512,.T.);
#17032=EDGE_CURVE('',#13686,#13687,#8513,.T.);
#17033=EDGE_CURVE('',#13687,#13688,#8514,.T.);
#17034=EDGE_CURVE('',#13688,#13689,#8515,.T.);
#17035=EDGE_CURVE('',#13689,#13684,#8516,.T.);
#17036=EDGE_CURVE('',#13679,#13682,#8517,.T.);
#17037=EDGE_CURVE('',#13690,#13691,#490,.T.);
#17038=EDGE_CURVE('',#13690,#13689,#8518,.T.);
#17039=EDGE_CURVE('',#13691,#13688,#8519,.T.);
#17040=EDGE_CURVE('',#13692,#13690,#491,.T.);
#17041=EDGE_CURVE('',#13692,#13684,#8520,.T.);
#17042=EDGE_CURVE('',#13693,#13692,#492,.T.);
#17043=EDGE_CURVE('',#13693,#13685,#8521,.T.);
#17044=EDGE_CURVE('',#13694,#13693,#493,.T.);
#17045=EDGE_CURVE('',#13686,#13694,#8522,.T.);
#17046=EDGE_CURVE('',#13691,#13695,#494,.T.);
#17047=EDGE_CURVE('',#13696,#13687,#8523,.T.);
#17048=EDGE_CURVE('',#13695,#13696,#495,.T.);
#17049=EDGE_CURVE('',#13696,#13694,#496,.T.);
#17050=EDGE_CURVE('',#13697,#13695,#8524,.T.);
#22228=ORIENTED_EDGE('',*,*,#17016,.T.);
#22229=ORIENTED_EDGE('',*,*,#17017,.T.);
#22230=ORIENTED_EDGE('',*,*,#17018,.T.);
#22231=ORIENTED_EDGE('',*,*,#17019,.T.);
#22232=ORIENTED_EDGE('',*,*,#17018,.F.);
#22233=ORIENTED_EDGE('',*,*,#17020,.F.);
#22234=ORIENTED_EDGE('',*,*,#17021,.F.);
#22235=ORIENTED_EDGE('',*,*,#17022,.T.);
#22236=ORIENTED_EDGE('',*,*,#17016,.F.);
#22237=ORIENTED_EDGE('',*,*,#17017,.F.);
#22238=ORIENTED_EDGE('',*,*,#17022,.F.);
#22239=ORIENTED_EDGE('',*,*,#17023,.T.);
#22240=ORIENTED_EDGE('',*,*,#17019,.F.);
#22241=ORIENTED_EDGE('',*,*,#17020,.T.);
#22242=ORIENTED_EDGE('',*,*,#17021,.T.);
#22243=ORIENTED_EDGE('',*,*,#17024,.T.);
#22244=ORIENTED_EDGE('',*,*,#17025,.T.);
#22245=ORIENTED_EDGE('',*,*,#17024,.F.);
#22246=ORIENTED_EDGE('',*,*,#17025,.F.);
#22247=ORIENTED_EDGE('',*,*,#17026,.T.);
#22248=ORIENTED_EDGE('',*,*,#17027,.T.);
#22249=ORIENTED_EDGE('',*,*,#17028,.T.);
#22250=ORIENTED_EDGE('',*,*,#17029,.T.);
#22251=ORIENTED_EDGE('',*,*,#17028,.F.);
#22252=ORIENTED_EDGE('',*,*,#17029,.F.);
#22253=ORIENTED_EDGE('',*,*,#17030,.T.);
#22254=ORIENTED_EDGE('',*,*,#17031,.T.);
#22255=ORIENTED_EDGE('',*,*,#17032,.T.);
#22256=ORIENTED_EDGE('',*,*,#17033,.T.);
#22257=ORIENTED_EDGE('',*,*,#17034,.T.);
#22258=ORIENTED_EDGE('',*,*,#17035,.T.);
#22259=ORIENTED_EDGE('',*,*,#17023,.F.);
#22260=ORIENTED_EDGE('',*,*,#17036,.T.);
#22261=ORIENTED_EDGE('',*,*,#17026,.F.);
#22262=ORIENTED_EDGE('',*,*,#17027,.F.);
#22263=ORIENTED_EDGE('',*,*,#17036,.F.);
#22264=ORIENTED_EDGE('',*,*,#17037,.F.);
#22265=ORIENTED_EDGE('',*,*,#17038,.T.);
#22266=ORIENTED_EDGE('',*,*,#17034,.F.);
#22267=ORIENTED_EDGE('',*,*,#17039,.F.);
#22268=ORIENTED_EDGE('',*,*,#17040,.F.);
#22269=ORIENTED_EDGE('',*,*,#17041,.T.);
#22270=ORIENTED_EDGE('',*,*,#17035,.F.);
#22271=ORIENTED_EDGE('',*,*,#17038,.F.);
#22272=ORIENTED_EDGE('',*,*,#17042,.F.);
#22273=ORIENTED_EDGE('',*,*,#17043,.T.);
#22274=ORIENTED_EDGE('',*,*,#17030,.F.);
#22275=ORIENTED_EDGE('',*,*,#17041,.F.);
#22276=ORIENTED_EDGE('',*,*,#17044,.F.);
#22277=ORIENTED_EDGE('',*,*,#17045,.F.);
#22278=ORIENTED_EDGE('',*,*,#17031,.F.);
#22279=ORIENTED_EDGE('',*,*,#17043,.F.);
#22280=ORIENTED_EDGE('',*,*,#17046,.F.);
#22281=ORIENTED_EDGE('',*,*,#17039,.T.);
#22282=ORIENTED_EDGE('',*,*,#17033,.F.);
#22283=ORIENTED_EDGE('',*,*,#17047,.F.);
#22284=ORIENTED_EDGE('',*,*,#17048,.F.);
#22285=ORIENTED_EDGE('',*,*,#17049,.F.);
#22286=ORIENTED_EDGE('',*,*,#17047,.T.);
#22287=ORIENTED_EDGE('',*,*,#17032,.F.);
#22288=ORIENTED_EDGE('',*,*,#17045,.T.);
#22289=ORIENTED_EDGE('',*,*,#17050,.T.);
#22290=ORIENTED_EDGE('',*,*,#17048,.T.);
#22291=ORIENTED_EDGE('',*,*,#17049,.T.);
#22292=ORIENTED_EDGE('',*,*,#17044,.T.);
#22293=ORIENTED_EDGE('',*,*,#17042,.T.);
#22294=ORIENTED_EDGE('',*,*,#17040,.T.);
#22295=ORIENTED_EDGE('',*,*,#17037,.T.);
#22296=ORIENTED_EDGE('',*,*,#17046,.T.);
#22297=ORIENTED_EDGE('',*,*,#17050,.F.);
#31169=PLANE('',#34457);
#31170=PLANE('',#34461);
#31171=PLANE('',#34467);
#31172=PLANE('',#34469);
#31173=PLANE('',#34470);
#31174=PLANE('',#34471);
#31175=PLANE('',#34472);
#31176=PLANE('',#34473);
#31177=PLANE('',#34474);
#32083=ADVANCED_FACE('',(#4402),#892,.F.);
#32084=ADVANCED_FACE('',(#4403),#1097,.T.);
#32085=ADVANCED_FACE('',(#4404,#1901),#31169,.T.);
#32086=ADVANCED_FACE('',(#4405),#569,.T.);
#32087=ADVANCED_FACE('',(#4406),#31170,.T.);
#32088=ADVANCED_FACE('',(#4407),#893,.T.);
#32089=ADVANCED_FACE('',(#4408,#1902),#31171,.T.);
#32090=ADVANCED_FACE('',(#4409),#1098,.T.);
#32091=ADVANCED_FACE('',(#4410),#31172,.F.);
#32092=ADVANCED_FACE('',(#4411),#31173,.F.);
#32093=ADVANCED_FACE('',(#4412),#31174,.F.);
#32094=ADVANCED_FACE('',(#4413),#31175,.F.);
#32095=ADVANCED_FACE('',(#4414),#31176,.F.);
#32096=ADVANCED_FACE('',(#4415),#31177,.F.);
#32097=ADVANCED_FACE('',(#4416),#570,.F.);
#33795=CLOSED_SHELL('',(#32083,#32084,#32085,#32086,#32087,#32088,#32089,
#32090,#32091,#32092,#32093,#32094,#32095,#32096,#32097));
#34448=AXIS2_PLACEMENT_3D('',#51138,#39001,#39002);
#34449=AXIS2_PLACEMENT_3D('',#51139,#39003,#39004);
#34450=AXIS2_PLACEMENT_3D('',#51142,#39005,#39006);
#34451=AXIS2_PLACEMENT_3D('',#51143,#39007,#39008);
#34452=AXIS2_PLACEMENT_3D('',#51145,#39009,#39010);
#34453=AXIS2_PLACEMENT_3D('',#51146,#39011,#39012);
#34454=AXIS2_PLACEMENT_3D('',#51147,#39013,#39014);
#34455=AXIS2_PLACEMENT_3D('',#51150,#39015,#39016);
#34456=AXIS2_PLACEMENT_3D('',#51151,#39017,#39018);
#34457=AXIS2_PLACEMENT_3D('',#51153,#39020,#39021);
#34458=AXIS2_PLACEMENT_3D('',#51155,#39022,#39023);
#34459=AXIS2_PLACEMENT_3D('',#51156,#39024,#39025);
#34460=AXIS2_PLACEMENT_3D('',#51159,#39027,#39028);
#34461=AXIS2_PLACEMENT_3D('',#51160,#39029,#39030);
#34462=AXIS2_PLACEMENT_3D('',#51161,#39031,#39032);
#34463=AXIS2_PLACEMENT_3D('',#51164,#39033,#39034);
#34464=AXIS2_PLACEMENT_3D('',#51165,#39035,#39036);
#34465=AXIS2_PLACEMENT_3D('',#51167,#39037,#39038);
#34466=AXIS2_PLACEMENT_3D('',#51168,#39039,#39040);
#34467=AXIS2_PLACEMENT_3D('',#51169,#39041,#39042);
#34468=AXIS2_PLACEMENT_3D('',#51182,#39049,#39050);
#34469=AXIS2_PLACEMENT_3D('',#51184,#39052,#39053);
#34470=AXIS2_PLACEMENT_3D('',#51192,#39056,#39057);
#34471=AXIS2_PLACEMENT_3D('',#51198,#39059,#39060);
#34472=AXIS2_PLACEMENT_3D('',#51204,#39062,#39063);
#34473=AXIS2_PLACEMENT_3D('',#51210,#39065,#39066);
#34474=AXIS2_PLACEMENT_3D('',#51220,#39068,#39069);
#34475=AXIS2_PLACEMENT_3D('',#51224,#39070,#39071);
#39001=DIRECTION('axis',(0.,0.,1.));
#39002=DIRECTION('refdir',(1.,0.,0.));
#39003=DIRECTION('center_axis',(1.14962333747911E-15,1.,1.12055937046026E-15));
#39004=DIRECTION('ref_axis',(1.,0.,0.));
#39005=DIRECTION('center_axis',(-1.14962333747911E-15,-1.,-1.12055937046026E-15));
#39006=DIRECTION('ref_axis',(5.33830693859541E-15,-1.12055937046026E-15,
1.));
#39007=DIRECTION('center_axis',(-1.14962333747911E-15,-1.,-1.12055937046026E-15));
#39008=DIRECTION('ref_axis',(5.33830693859541E-15,-1.12055937046026E-15,
1.));
#39009=DIRECTION('center_axis',(0.,1.12055937046026E-15,-1.));
#39010=DIRECTION('ref_axis',(-1.,0.,0.));
#39011=DIRECTION('center_axis',(1.14962333747911E-15,1.,1.12055937046026E-15));
#39012=DIRECTION('ref_axis',(5.33830693859542E-15,-1.12055937046026E-15,
1.));
#39013=DIRECTION('center_axis',(1.14962333747911E-15,1.,1.12055937046026E-15));
#39014=DIRECTION('ref_axis',(-5.46077161851015E-15,1.12055937046026E-15,
-1.));
#39015=DIRECTION('center_axis',(1.14962333747911E-15,1.,1.12055937046026E-15));
#39016=DIRECTION('ref_axis',(5.46077161851015E-15,-1.12055937046026E-15,
1.));
#39017=DIRECTION('center_axis',(1.14962333747911E-15,1.,1.12055937046026E-15));
#39018=DIRECTION('ref_axis',(5.46077161851015E-15,-1.12055937046026E-15,
1.));
#39019=DIRECTION('',(-1.14962333747911E-15,-1.,-1.12055937046026E-15));
#39020=DIRECTION('center_axis',(1.14962333747911E-15,1.,1.12055937046026E-15));
#39021=DIRECTION('ref_axis',(1.,-1.1496233374791E-15,-5.46077161851015E-15));
#39022=DIRECTION('center_axis',(1.14962333747911E-15,1.,1.12055937046026E-15));
#39023=DIRECTION('ref_axis',(-5.46077161851015E-15,1.12055937046026E-15,
-1.));
#39024=DIRECTION('center_axis',(-1.14962333747911E-15,-1.,-1.12055937046026E-15));
#39025=DIRECTION('ref_axis',(5.46077161851015E-15,-1.12055937046026E-15,
1.));
#39026=DIRECTION('',(4.5876594940778E-15,0.707106781186547,0.707106781186548));
#39027=DIRECTION('center_axis',(-1.14962333747911E-15,-1.,-1.12055937046026E-15));
#39028=DIRECTION('ref_axis',(5.46077161851015E-15,-1.12055937046026E-15,
1.));
#39029=DIRECTION('center_axis',(1.14962333747911E-15,1.,1.12055937046026E-15));
#39030=DIRECTION('ref_axis',(1.,-1.1496233374791E-15,-5.46077161851015E-15));
#39031=DIRECTION('center_axis',(1.14962333747911E-15,1.,1.12055937046026E-15));
#39032=DIRECTION('ref_axis',(1.,0.,-7.105427357601E-15));
#39033=DIRECTION('center_axis',(-1.14962333747911E-15,-1.,-1.12055937046026E-15));
#39034=DIRECTION('ref_axis',(5.33830693859541E-15,-1.12055937046026E-15,
1.));
#39035=DIRECTION('center_axis',(-1.14962333747911E-15,-1.,-1.12055937046026E-15));
#39036=DIRECTION('ref_axis',(5.33830693859541E-15,-1.12055937046026E-15,
1.));
#39037=DIRECTION('center_axis',(8.88178419700128E-15,-1.12055937046027E-15,
1.));
#39038=DIRECTION('ref_axis',(-1.,0.,8.88178419700128E-15));
#39039=DIRECTION('center_axis',(1.14962333747911E-15,1.,1.12055937046026E-15));
#39040=DIRECTION('ref_axis',(5.33830693859541E-15,-1.12055937046026E-15,
1.));
#39041=DIRECTION('center_axis',(-1.14962333747911E-15,-1.,-1.12055937046026E-15));
#39042=DIRECTION('ref_axis',(-1.,1.1496233374791E-15,5.46077161851015E-15));
#39043=DIRECTION('',(-1.,1.1496233374791E-15,4.98003094691426E-15));
#39044=DIRECTION('',(-0.499999999999995,-3.95621212527735E-16,0.866025403784441));
#39045=DIRECTION('',(0.500000000000005,-1.54524455000684E-15,0.866025403784436));
#39046=DIRECTION('',(1.,-1.1496233374791E-15,-5.34058645061118E-15));
#39047=DIRECTION('',(0.499999999999995,3.95621212527734E-16,-0.866025403784441));
#39048=DIRECTION('',(-0.500000000000005,1.54524455000684E-15,-0.866025403784436));
#39049=DIRECTION('center_axis',(1.14962333747911E-15,1.,1.12055937046026E-15));
#39050=DIRECTION('ref_axis',(-5.46077161851015E-15,1.12055937046026E-15,
-1.));
#39051=DIRECTION('',(-1.14962333747911E-15,-1.,-1.12055937046026E-15));
#39052=DIRECTION('center_axis',(0.866025403784442,-1.55588270027048E-15,
0.499999999999995));
#39053=DIRECTION('ref_axis',(-1.14974466254757E-15,-1.,-1.12034922927745E-15));
#39054=DIRECTION('',(-1.14962333747911E-15,-1.,-1.12055937046026E-15));
#39055=DIRECTION('',(-1.14962333747911E-15,-1.,-1.12055937046026E-15));
#39056=DIRECTION('center_axis',(0.866025403784436,-4.35323329810222E-16,
-0.500000000000005));
#39057=DIRECTION('ref_axis',(-1.14950201241065E-15,-1.,-1.12034922927745E-15));
#39058=DIRECTION('',(-1.14962333747911E-15,-1.,-1.12055937046026E-15));
#39059=DIRECTION('center_axis',(-4.98003094691426E-15,1.12055937046026E-15,
-1.));
#39060=DIRECTION('ref_axis',(-1.,1.1496233374791E-15,4.98003094691426E-15));
#39061=DIRECTION('',(-1.14962333747911E-15,-1.,-1.12055937046026E-15));
#39062=DIRECTION('center_axis',(-0.866025403784442,1.55588270027048E-15,
-0.499999999999995));
#39063=DIRECTION('ref_axis',(1.14974466254757E-15,1.,1.12034922927745E-15));
#39064=DIRECTION('',(1.14962333747911E-15,1.,1.12055937046026E-15));
#39065=DIRECTION('center_axis',(5.34058645061118E-15,-1.12055937046026E-15,
1.));
#39066=DIRECTION('ref_axis',(1.,-1.1496233374791E-15,-5.34058645061118E-15));
#39067=DIRECTION('',(-1.14962333747911E-15,-1.,-1.12055937046026E-15));
#39068=DIRECTION('center_axis',(-0.866025403784436,4.35323329810222E-16,
0.500000000000005));
#39069=DIRECTION('ref_axis',(1.14950201241065E-15,1.,1.12034922927745E-15));
#39070=DIRECTION('center_axis',(-1.14962333747911E-15,-1.,-1.12055937046026E-15));
#39071=DIRECTION('ref_axis',(-5.46077161851015E-15,1.12055937046026E-15,
-1.));
#39072=DIRECTION('',(4.04829775328281E-15,-0.500000000000001,0.866025403784438));
#51138=CARTESIAN_POINT('',(0.,0.,0.));
#51139=CARTESIAN_POINT('Origin',(416.615917770968,-291.37200726879,403.500000551892));
#51140=CARTESIAN_POINT('',(411.615917770968,-291.37200726879,403.500000551892));
#51141=CARTESIAN_POINT('',(416.615917770968,-291.37200726879,408.500000551892));
#51142=CARTESIAN_POINT('Origin',(416.615917770968,-291.37200726879,403.500000551892));
#51143=CARTESIAN_POINT('Origin',(416.615917770968,-291.37200726879,403.500000551892));
#51144=CARTESIAN_POINT('',(411.515917770968,-291.47200726879,403.500000551892));
#51145=CARTESIAN_POINT('Origin',(411.515917770968,-291.37200726879,403.500000551892));
#51146=CARTESIAN_POINT('Origin',(416.615917770968,-291.47200726879,403.500000551892));
#51147=CARTESIAN_POINT('Origin',(416.615917770968,-274.47200726879,403.500000551892));
#51148=CARTESIAN_POINT('',(416.615917770968,-262.39218226879,398.500000551892));
#51149=CARTESIAN_POINT('',(416.615917770968,-262.39218226879,408.500000551892));
#51150=CARTESIAN_POINT('Origin',(416.615917770968,-262.39218226879,403.500000551892));
#51151=CARTESIAN_POINT('Origin',(416.615917770968,-262.39218226879,403.500000551892));
#51152=CARTESIAN_POINT('',(416.615917770968,-274.47200726879,408.500000551892));
#51153=CARTESIAN_POINT('Origin',(416.615917770968,-291.47200726879,397.000000551892));
#51154=CARTESIAN_POINT('',(416.615917770968,-291.47200726879,411.500000551892));
#51155=CARTESIAN_POINT('Origin',(416.615917770968,-291.47200726879,403.500000551892));
#51156=CARTESIAN_POINT('Origin',(416.615917770968,-261.93209476879,403.500000551892));
#51157=CARTESIAN_POINT('',(416.615917770968,-261.47200726879,399.420175551892));
#51158=CARTESIAN_POINT('',(416.615917770968,-261.93209476879,398.960088051892));
#51159=CARTESIAN_POINT('Origin',(416.615917770968,-261.47200726879,403.500000551892));
#51160=CARTESIAN_POINT('Origin',(416.615917770968,-261.47200726879,401.000000551892));
#51161=CARTESIAN_POINT('Origin',(416.615917770968,-300.47200726879,403.500000551892));
#51162=CARTESIAN_POINT('',(408.615917770968,-300.47200726879,403.500000551892));
#51163=CARTESIAN_POINT('',(416.615917770968,-300.47200726879,411.500000551892));
#51164=CARTESIAN_POINT('Origin',(416.615917770968,-300.47200726879,403.500000551892));
#51165=CARTESIAN_POINT('Origin',(416.615917770968,-300.47200726879,403.500000551892));
#51166=CARTESIAN_POINT('',(409.615917770968,-301.47200726879,403.500000551892));
#51167=CARTESIAN_POINT('Origin',(409.615917770968,-300.47200726879,403.500000551892));
#51168=CARTESIAN_POINT('Origin',(416.615917770968,-301.47200726879,403.500000551892));
#51169=CARTESIAN_POINT('Origin',(416.615917770968,-301.47200726879,397.190599475133));
#51170=CARTESIAN_POINT('',(418.925318847726,-301.47200726879,399.500000551892));
#51171=CARTESIAN_POINT('',(414.306516694209,-301.47200726879,399.500000551892));
#51172=CARTESIAN_POINT('',(415.461217232588,-301.47200726879,399.500000551892));
#51173=CARTESIAN_POINT('',(411.997115617451,-301.47200726879,403.500000551892));
#51174=CARTESIAN_POINT('',(412.57446588664,-301.47200726879,402.500000551892));
#51175=CARTESIAN_POINT('',(414.306516694209,-301.47200726879,407.500000551892));
#51176=CARTESIAN_POINT('',(413.72916642502,-301.47200726879,406.500000551892));
#51177=CARTESIAN_POINT('',(418.925318847726,-301.47200726879,407.500000551892));
#51178=CARTESIAN_POINT('',(417.770618309347,-301.47200726879,407.500000551892));
#51179=CARTESIAN_POINT('',(421.234719924485,-301.47200726879,403.500000551892));
#51180=CARTESIAN_POINT('',(420.657369655295,-301.47200726879,404.500000551892));
#51181=CARTESIAN_POINT('',(419.502669116916,-301.47200726879,400.500000551892));
#51182=CARTESIAN_POINT('Origin',(416.615917770968,-296.47200726879,403.500000551892));
#51183=CARTESIAN_POINT('',(416.615917770968,-296.47200726879,411.500000551892));
#51184=CARTESIAN_POINT('Origin',(421.234719924485,-301.47200726879,403.500000551892));
#51185=CARTESIAN_POINT('',(421.234719924485,-296.47200726879,403.500000551892));
#51186=CARTESIAN_POINT('',(418.925318847726,-296.47200726879,407.500000551892));
#51187=CARTESIAN_POINT('Ctrl Pts',(421.234719924485,-296.47200726879,403.500000551892));
#51188=CARTESIAN_POINT('Ctrl Pts',(420.080019386106,-295.805340602123,405.500000551892));
#51189=CARTESIAN_POINT('Ctrl Pts',(418.925318847726,-296.47200726879,407.500000551892));
#51190=CARTESIAN_POINT('',(421.234719924485,-298.97200726879,403.500000551892));
#51191=CARTESIAN_POINT('',(418.925318847726,-298.97200726879,407.500000551892));
#51192=CARTESIAN_POINT('Origin',(418.925318847726,-301.47200726879,399.500000551892));
#51193=CARTESIAN_POINT('',(418.925318847726,-296.47200726879,399.500000551892));
#51194=CARTESIAN_POINT('Ctrl Pts',(418.925318847726,-296.47200726879,399.500000551892));
#51195=CARTESIAN_POINT('Ctrl Pts',(420.080019386106,-295.805340602123,401.500000551892));
#51196=CARTESIAN_POINT('Ctrl Pts',(421.234719924485,-296.47200726879,403.500000551892));
#51197=CARTESIAN_POINT('',(418.925318847726,-298.97200726879,399.500000551892));
#51198=CARTESIAN_POINT('Origin',(414.306516694209,-301.47200726879,399.500000551892));
#51199=CARTESIAN_POINT('',(414.306516694209,-296.47200726879,399.500000551892));
#51200=CARTESIAN_POINT('Ctrl Pts',(414.306516694209,-296.47200726879,399.500000551892));
#51201=CARTESIAN_POINT('Ctrl Pts',(416.615917770968,-295.805340602123,399.500000551892));
#51202=CARTESIAN_POINT('Ctrl Pts',(418.925318847726,-296.47200726879,399.500000551892));
#51203=CARTESIAN_POINT('',(414.306516694209,-298.97200726879,399.500000551892));
#51204=CARTESIAN_POINT('Origin',(411.997115617451,-301.47200726879,403.500000551892));
#51205=CARTESIAN_POINT('',(411.997115617451,-296.47200726879,403.500000551892));
#51206=CARTESIAN_POINT('Ctrl Pts',(411.997115617451,-296.47200726879,403.500000551892));
#51207=CARTESIAN_POINT('Ctrl Pts',(413.15181615583,-295.805340602123,401.500000551892));
#51208=CARTESIAN_POINT('Ctrl Pts',(414.306516694209,-296.47200726879,399.500000551892));
#51209=CARTESIAN_POINT('',(411.997115617451,-298.97200726879,403.500000551892));
#51210=CARTESIAN_POINT('Origin',(418.925318847726,-301.47200726879,407.500000551892));
#51211=CARTESIAN_POINT('',(416.615917770968,-296.114741678882,407.500000551892));
#51212=CARTESIAN_POINT('Ctrl Pts',(418.925318847726,-296.47200726879,407.500000551892));
#51213=CARTESIAN_POINT('Ctrl Pts',(417.687714540692,-296.114741678882,407.500000551892));
#51214=CARTESIAN_POINT('Ctrl Pts',(416.615917770968,-296.114741678882,407.500000551892));
#51215=CARTESIAN_POINT('',(414.306516694209,-296.47200726879,407.500000551892));
#51216=CARTESIAN_POINT('',(414.306516694209,-298.97200726879,407.500000551892));
#51217=CARTESIAN_POINT('Ctrl Pts',(416.615917770968,-296.114741678882,407.500000551892));
#51218=CARTESIAN_POINT('Ctrl Pts',(415.544121001243,-296.114741678882,407.500000551892));
#51219=CARTESIAN_POINT('Ctrl Pts',(414.306516694209,-296.47200726879,407.500000551892));
#51220=CARTESIAN_POINT('Origin',(414.306516694209,-301.47200726879,407.500000551892));
#51221=CARTESIAN_POINT('Ctrl Pts',(414.306516694209,-296.47200726879,407.500000551892));
#51222=CARTESIAN_POINT('Ctrl Pts',(413.15181615583,-295.805340602123,405.500000551892));
#51223=CARTESIAN_POINT('Ctrl Pts',(411.997115617451,-296.47200726879,403.500000551892));
#51224=CARTESIAN_POINT('Origin',(416.615917770968,-295.138673935457,403.500000551892));
#51225=CARTESIAN_POINT('',(416.615917770968,-293.805340602123,403.500000551892));
#51226=CARTESIAN_POINT('',(416.615917770968,-295.138673935457,405.80940162865));
#61755=UNCERTAINTY_MEASURE_WITH_UNIT(LENGTH_MEASURE(0.01),#61812,
'DISTANCE_ACCURACY_VALUE',
'Maximum model space distance between geometric entities at asserted c
onnectivities');
#61780=UNCERTAINTY_MEASURE_WITH_UNIT(LENGTH_MEASURE(0.01),#61812,
'DISTANCE_ACCURACY_VALUE',
'Maximum model space distance between geometric entities at asserted c
onnectivities');
#61786=(
GEOMETRIC_REPRESENTATION_CONTEXT(3)
GLOBAL_UNCERTAINTY_ASSIGNED_CONTEXT((#61755))
GLOBAL_UNIT_ASSIGNED_CONTEXT((#61812,#61814,#61815))
REPRESENTATION_CONTEXT('','3D')
);
#61811=(
GEOMETRIC_REPRESENTATION_CONTEXT(3)
GLOBAL_UNCERTAINTY_ASSIGNED_CONTEXT((#61780))
GLOBAL_UNIT_ASSIGNED_CONTEXT((#61812,#61814,#61815))
REPRESENTATION_CONTEXT('','3D')
);
#61812=(
LENGTH_UNIT()
NAMED_UNIT(*)
SI_UNIT(.MILLI.,.METRE.)
);
#61814=(
NAMED_UNIT(*)
PLANE_ANGLE_UNIT()
SI_UNIT($,.RADIAN.)
);
#61815=(
NAMED_UNIT(*)
SI_UNIT($,.STERADIAN.)
SOLID_ANGLE_UNIT()
);
#61821=SHAPE_DEFINITION_REPRESENTATION(#61851,#61973);
#61851=PRODUCT_DEFINITION_SHAPE('',$,#62004);
#61973=SHAPE_REPRESENTATION('',(#34448),#61786);
#61998=PRODUCT_DEFINITION_CONTEXT('part definition',#62090,'design');
#62004=PRODUCT_DEFINITION('Extended Housing Socket Screw',
'Extended Housing Socket Screw',#62034,#61998);
#62034=PRODUCT_DEFINITION_FORMATION('',$,#62097);
#62090=APPLICATION_CONTEXT('Managed model based 3d engineering');
#62091=PRODUCT_CONTEXT('part definition',#62090,'mechanical');
#62097=PRODUCT('Extended Housing Socket Screw',
'Extended Housing Socket Screw',$,(#62091));
#62157=COLOUR_RGB('Black',0.12,0.14,0.17);
#62158=FILL_AREA_STYLE_COLOUR('',#62157);
#62159=FILL_AREA_STYLE('',(#62158));
#62160=SURFACE_STYLE_FILL_AREA(#62159);
#62161=SURFACE_SIDE_STYLE('',(#62160));
#62162=SURFACE_STYLE_USAGE(.BOTH.,#62161);
#62163=PRESENTATION_STYLE_ASSIGNMENT((#62162));
ENDSEC;
END-ISO-10303-21;
